ISO-10303-21;
HEADER;
FILE_DESCRIPTION (('STEP AP214'),
    '1' );
FILE_NAME ('Eraser.step',
    '2026-10-06T14:00:01',
    ( '' ),
    ( '' ),
    'SwSTEP 2.0',
    'SolidWorks 2020',
    '' );
FILE_SCHEMA (( 'AUTOMOTIVE_DESIGN' ));
ENDSEC;

DATA;
#48=( NAMED_UNIT ( * ) PLANE_ANGLE_UNIT ( ) SI_UNIT ( $, .RADIAN. ) );
#300=DIRECTION ( 'NONE',  ( 0.000000000000000000, 1.224646799147353454E-16, 1.000000000000000000 ) ) ;
#428=DIRECTION ( 'NONE',  ( -1.000000000000000000, -0.000000000000000000, 3.491481338843133750E-15 ) ) ;
#489=VERTEX_POINT ( 'NONE', #20441 ) ;
#654=EDGE_LOOP ( 'NONE', ( #9080, #23435, #20814, #9552 ) ) ;
#703=ORIENTED_EDGE ( 'NONE', *, *, #18963, .T. ) ;
#706=ORIENTED_EDGE ( 'NONE', *, *, #12889, .T. ) ;
#765=AXIS2_PLACEMENT_3D ( 'NONE', #16455, #26113, #4724 ) ;
#772=ORIENTED_EDGE ( 'NONE', *, *, #1502, .T. ) ;
#1149=EDGE_LOOP ( 'NONE', ( #1743, #772, #703, #19736 ) ) ;
#1377=AXIS2_PLACEMENT_3D ( 'NONE', #1548, #23572, #11690 ) ;
#1496=ADVANCED_FACE ( 'NONE', ( #16639 ), #8842, .T. ) ;
#1502=EDGE_CURVE ( 'NONE', #489, #27700, #9332, .T. ) ;
#1548=CARTESIAN_POINT ( 'NONE',  ( 51.50000000000002132, 1.163569835200988601E-28, -1.798112889504214751E-13 ) ) ;
#1557=EDGE_LOOP ( 'NONE', ( #27377, #4605, #25802, #28932 ) ) ;
#1716=DIRECTION ( 'NONE',  ( 0.000000000000000000, 0.000000000000000000, -1.000000000000000000 ) ) ;
#1743=ORIENTED_EDGE ( 'NONE', *, *, #9646, .F. ) ;
#1828=AXIS2_PLACEMENT_3D ( 'NONE', #2424, #26330, #19224 ) ;
#2241=AXIS2_PLACEMENT_3D ( 'NONE', #20904, #4257, #28659 ) ;
#2400=TOROIDAL_SURFACE ( 'NONE', #11510, 1.375000000000001332, 0.2500000000000000000 ) ;
#2413=VECTOR ( 'NONE', #23951, 1000.000000000000000 ) ;
#2424=CARTESIAN_POINT ( 'NONE',  ( 51.50000000000001421, 1.163569835200988601E-28, -1.375000000000181188 ) ) ;
#2599=EDGE_LOOP ( 'NONE', ( #17167, #21447 ) ) ;
#2650=LINE ( 'NONE', #22137, #12906 ) ;
#2671=CARTESIAN_POINT ( 'NONE',  ( 64.00000000000001421, 1.163569835200988601E-28, -2.234548056859606357E-13 ) ) ;
#3172=( NAMED_UNIT ( * ) PLANE_ANGLE_UNIT ( ) SI_UNIT ( $, .RADIAN. ) );
#3333=SURFACE_SIDE_STYLE ('',( #10618 ) ) ;
#3391=CARTESIAN_POINT ( 'NONE',  ( 51.50000000000002132, 1.163569835200988601E-28, -1.798112889504214751E-13 ) ) ;
#3424=TOROIDAL_SURFACE ( 'NONE', #29206, 1.375000000000001332, 0.2500000000000000000 ) ;
#3751=DIRECTION ( 'NONE',  ( 1.000000000000000000, 0.000000000000000000, -3.491481338843133355E-15 ) ) ;
#3807=EDGE_CURVE ( 'NONE', #24533, #27460, #23472, .T. ) ;
#4040=PRODUCT_DEFINITION_FORMATION_WITH_SPECIFIED_SOURCE ( 'ANY', '', #15367, .NOT_KNOWN. ) ;
#4257=DIRECTION ( 'NONE',  ( -1.000000000000000000, -0.000000000000000000, 3.491481338843133750E-15 ) ) ;
#4295=AXIS2_PLACEMENT_3D ( 'NONE', #16013, #10791, #11105 ) ;
#4343=CARTESIAN_POINT ( 'NONE',  ( 64.25000000000001421, 1.836970198722195229E-16, 1.374999999999777067 ) ) ;
#4428=CIRCLE ( 'NONE', #9999, 1.625000000000001332 ) ;
#4605=ORIENTED_EDGE ( 'NONE', *, *, #13802, .T. ) ;
#4724=DIRECTION ( 'NONE',  ( -3.491481338843133355E-15, 0.000000000000000000, -1.000000000000000000 ) ) ;
#4948=( NAMED_UNIT ( * ) SI_UNIT ( $, .STERADIAN. ) SOLID_ANGLE_UNIT ( ) );
#5496=PLANE ( 'NONE',  #16590 ) ;
#5558=SURFACE_STYLE_USAGE ( .BOTH. , #3333 ) ;
#6145=DIRECTION ( 'NONE',  ( -3.491481338843133355E-15, 0.000000000000000000, -1.000000000000000000 ) ) ;
#6237=ORIENTED_EDGE ( 'NONE', *, *, #28141, .T. ) ;
#6330=TOROIDAL_SURFACE ( 'NONE', #765, 1.375000000000001332, 0.2500000000000000000 ) ;
#6643=SHAPE_DEFINITION_REPRESENTATION ( #17390, #30888 ) ;
#6699=CARTESIAN_POINT ( 'NONE',  ( 51.25000000000001421, 1.163569835200988601E-28, -1.789384186157106949E-13 ) ) ;
#6757=ORIENTED_EDGE ( 'NONE', *, *, #17649, .F. ) ;
#6975=ORIENTED_EDGE ( 'NONE', *, *, #3807, .T. ) ;
#7030=DIRECTION ( 'NONE',  ( -1.000000000000000000, -0.000000000000000000, 3.491481338843133355E-15 ) ) ;
#7076=ORIENTED_EDGE ( 'NONE', *, *, #3807, .F. ) ;
#7306=DIRECTION ( 'NONE',  ( 0.000000000000000000, 0.000000000000000000, 1.000000000000000000 ) ) ;
#7323=CARTESIAN_POINT ( 'NONE',  ( 51.25000000000001421, 1.163569835200988601E-28, -1.375000000000180300 ) ) ;
#7396=STYLED_ITEM ( 'NONE', ( #18274 ), #15704 ) ;
#7458=ORIENTED_EDGE ( 'NONE', *, *, #10557, .T. ) ;
#7937=( GEOMETRIC_REPRESENTATION_CONTEXT ( 3 ) GLOBAL_UNCERTAINTY_ASSIGNED_CONTEXT ( ( #24385 ) ) GLOBAL_UNIT_ASSIGNED_CONTEXT ( ( #13495, #48, #4948 ) ) REPRESENTATION_CONTEXT ( 'NONE', 'WORKASPACE' ) );
#8225=DIRECTION ( 'NONE',  ( 1.000000000000000000, 0.000000000000000000, -3.491481338843133355E-15 ) ) ;
#8236=PRESENTATION_STYLE_ASSIGNMENT (( #5558 ) ) ;
#8287=DIRECTION ( 'NONE',  ( -3.491481338843133355E-15, 0.000000000000000000, -1.000000000000000000 ) ) ;
#8448=FACE_OUTER_BOUND ( 'NONE', #30940, .T. ) ;
#8515=PLANE ( 'NONE',  #14960 ) ;
#8598=SURFACE_STYLE_USAGE ( .BOTH. , #30287 ) ;
#8842=CYLINDRICAL_SURFACE ( 'NONE', #2241, 1.625000000000001332 ) ;
#8945=DIRECTION ( 'NONE',  ( -4.275831445896958607E-31, 1.000000000000000000, -1.224646799147353207E-16 ) ) ;
#9018=AXIS2_PLACEMENT_3D ( 'NONE', #25987, #9060, #11596 ) ;
#9060=DIRECTION ( 'NONE',  ( 0.000000000000000000, 0.000000000000000000, 1.000000000000000000 ) ) ;
#9080=ORIENTED_EDGE ( 'NONE', *, *, #13802, .F. ) ;
#9332=CIRCLE ( 'NONE', #13338, 1.625000000000001332 ) ;
#9354=CARTESIAN_POINT ( 'NONE',  ( 64.00000000000001421, 1.163569835200988601E-28, 1.624999999999777955 ) ) ;
#9446=CIRCLE ( 'NONE', #24085, 1.375000000000001332 ) ;
#9552=ORIENTED_EDGE ( 'NONE', *, *, #24207, .F. ) ;
#9583=MECHANICAL_DESIGN_GEOMETRIC_PRESENTATION_REPRESENTATION('',(#21721),#27250);
#9646=EDGE_CURVE ( 'NONE', #489, #21323, #19218, .T. ) ;
#9826=AXIS2_PLACEMENT_3D ( 'NONE', #6699, #7030, #16359 ) ;
#9914=ORIENTED_EDGE ( 'NONE', *, *, #17649, .T. ) ;
#9999=AXIS2_PLACEMENT_3D ( 'NONE', #2671, #12466, #29269 ) ;
#10121=EDGE_CURVE ( 'NONE', #27460, #21323, #30644, .T. ) ;
#10129=ORIENTED_EDGE ( 'NONE', *, *, #10121, .F. ) ;
#10557=EDGE_CURVE ( 'NONE', #27460, #24533, #9446, .T. ) ;
#10618=SURFACE_STYLE_FILL_AREA ( #13135 ) ;
#10791=DIRECTION ( 'NONE',  ( 1.000000000000000000, 0.000000000000000000, -3.491481338843133355E-15 ) ) ;
#10882=TOROIDAL_SURFACE ( 'NONE', #24532, 1.375000000000001332, 0.2500000000000000000 ) ;
#10981=FILL_AREA_STYLE ('',( #23018 ) ) ;
#11105=DIRECTION ( 'NONE',  ( 0.000000000000000000, 0.000000000000000000, -1.000000000000000000 ) ) ;
#11290=ORIENTED_EDGE ( 'NONE', *, *, #18963, .F. ) ;
#11358=ORIENTED_EDGE ( 'NONE', *, *, #10557, .F. ) ;
#11431=AXIS2_PLACEMENT_3D ( 'NONE', #23324, #13788, #26792 ) ;
#11437=MECHANICAL_DESIGN_GEOMETRIC_PRESENTATION_REPRESENTATION('',(#7396),#7937);
#11510=AXIS2_PLACEMENT_3D ( 'NONE', #25231, #18275, #8287 ) ;
#11596=DIRECTION ( 'NONE',  ( 1.000000000000000000, 0.000000000000000000, 0.000000000000000000 ) ) ;
#11690=DIRECTION ( 'NONE',  ( -4.270088556250598741E-15, 0.000000000000000000, -1.000000000000000000 ) ) ;
#11868=DIRECTION ( 'NONE',  ( -4.275831445896958607E-31, 1.000000000000000000, -1.224646799147353207E-16 ) ) ;
#12006=CIRCLE ( 'NONE', #20609, 0.2500000000000000000 ) ;
#12069=FACE_OUTER_BOUND ( 'NONE', #1149, .T. ) ;
#12365=CIRCLE ( 'NONE', #17441, 0.2500000000000000000 ) ;
#12466=DIRECTION ( 'NONE',  ( -1.000000000000000000, -0.000000000000000000, 3.491481338843133355E-15 ) ) ;
#12573=COLOUR_RGB ( '', 0.09019608, 0.27058824, 0.51372549) ;
#12726=EDGE_LOOP ( 'NONE', ( #706, #16064, #6237, #11290 ) ) ;
#12889=EDGE_CURVE ( 'NONE', #27700, #489, #4428, .T. ) ;
#12906=VECTOR ( 'NONE', #428, 1000.000000000000000 ) ;
#12983=SHAPE_REPRESENTATION_RELATIONSHIP ( 'NONE' , 'NONE' ,  #30888, #13430 ) ;
#13077=ADVANCED_FACE ( 'NONE', ( #17713 ), #3424, .T. ) ;
#13135=FILL_AREA_STYLE ('',( #25332 ) ) ;
#13184=DIRECTION ( 'NONE',  ( -3.491481338843133355E-15, 0.000000000000000000, -1.000000000000000000 ) ) ;
#13303=ADVANCED_FACE ( 'NONE', ( #8448 ), #2400, .T. ) ;
#13338=AXIS2_PLACEMENT_3D ( 'NONE', #13747, #26432, #1716 ) ;
#13430=ADVANCED_BREP_SHAPE_REPRESENTATION ( '', ( #15704, #9018 ), #18167 ) ;
#13495=( LENGTH_UNIT ( ) NAMED_UNIT ( * ) SI_UNIT ( .MILLI., .METRE. ) );
#13747=CARTESIAN_POINT ( 'NONE',  ( 64.00000000000001421, 1.163569835200988601E-28, -2.234548056859606357E-13 ) ) ;
#13788=DIRECTION ( 'NONE',  ( 1.000000000000000000, 0.000000000000000000, -3.491481338843133355E-15 ) ) ;
#13802=EDGE_CURVE ( 'NONE', #27700, #16231, #28202, .T. ) ;
#13882=CIRCLE ( 'NONE', #4295, 1.375000000000001332 ) ;
#14249=CARTESIAN_POINT ( 'NONE',  ( 51.25000000000001421, 1.163569835200988601E-28, -1.789384186157106949E-13 ) ) ;
#14274=CYLINDRICAL_SURFACE ( 'NONE', #28608, 1.625000000000001332 ) ;
#14683=CARTESIAN_POINT ( 'NONE',  ( 64.25000000000001421, 1.163569835200988601E-28, -2.243276760206714411E-13 ) ) ;
#14692=DIRECTION ( 'NONE',  ( 0.000000000000000000, 0.000000000000000000, -1.000000000000000000 ) ) ;
#14960=AXIS2_PLACEMENT_3D ( 'NONE', #27505, #3751, #6145 ) ;
#14992=DIRECTION ( 'NONE',  ( 0.000000000000000000, -1.000000000000000000, -0.000000000000000000 ) ) ;
#15208=( LENGTH_UNIT ( ) NAMED_UNIT ( * ) SI_UNIT ( .MILLI., .METRE. ) );
#15355=( LENGTH_UNIT ( ) NAMED_UNIT ( * ) SI_UNIT ( .MILLI., .METRE. ) );
#15367=PRODUCT ( 'Eraser', 'Eraser', '', ( #28337 ) ) ;
#15514=CARTESIAN_POINT ( 'NONE',  ( 64.25000000000001421, 1.163569835200988601E-28, -2.243276760206714411E-13 ) ) ;
#15704=MANIFOLD_SOLID_BREP ( 'Stock-MAS-683-1', #26666 ) ;
#16013=CARTESIAN_POINT ( 'NONE',  ( 64.25000000000001421, 1.163569835200988601E-28, -2.243276760206714411E-13 ) ) ;
#16064=ORIENTED_EDGE ( 'NONE', *, *, #9646, .T. ) ;
#16231=VERTEX_POINT ( 'NONE', #4343 ) ;
#16298=EDGE_LOOP ( 'NONE', ( #6757, #11358, #17834, #19421 ) ) ;
#16359=DIRECTION ( 'NONE',  ( -5.046468293750706671E-15, 0.000000000000000000, -1.000000000000000000 ) ) ;
#16455=CARTESIAN_POINT ( 'NONE',  ( 64.00000000000001421, 1.163569835200988601E-28, -2.234548056859606357E-13 ) ) ;
#16590=AXIS2_PLACEMENT_3D ( 'NONE', #14683, #21978, #22142 ) ;
#16639=FACE_OUTER_BOUND ( 'NONE', #12726, .T. ) ;
#16792=CARTESIAN_POINT ( 'NONE',  ( 64.00000000000001421, 1.683889348828776048E-16, 1.374999999999777955 ) ) ;
#17034=AXIS2_PLACEMENT_3D ( 'NONE', #16792, #11868, #300 ) ;
#17155=EDGE_CURVE ( 'NONE', #26979, #21323, #23558, .T. ) ;
#17167=ORIENTED_EDGE ( 'NONE', *, *, #21805, .T. ) ;
#17390=PRODUCT_DEFINITION_SHAPE ( 'NONE', 'NONE',  #26371 ) ;
#17401=AXIS2_PLACEMENT_3D ( 'NONE', #15514, #8225, #22815 ) ;
#17441=AXIS2_PLACEMENT_3D ( 'NONE', #31109, #8945, #28751 ) ;
#17649=EDGE_CURVE ( 'NONE', #24533, #26979, #12365, .T. ) ;
#17713=FACE_OUTER_BOUND ( 'NONE', #654, .T. ) ;
#17755=( NAMED_UNIT ( * ) SI_UNIT ( $, .STERADIAN. ) SOLID_ANGLE_UNIT ( ) );
#17834=ORIENTED_EDGE ( 'NONE', *, *, #10121, .T. ) ;
#18022=ADVANCED_FACE ( 'NONE', ( #25061 ), #10882, .T. ) ;
#18052=UNCERTAINTY_MEASURE_WITH_UNIT (LENGTH_MEASURE( 1.000000000000000082E-05 ), #15208, 'distance_accuracy_value', 'NONE');
#18167=( GEOMETRIC_REPRESENTATION_CONTEXT ( 3 ) GLOBAL_UNCERTAINTY_ASSIGNED_CONTEXT ( ( #24075 ) ) GLOBAL_UNIT_ASSIGNED_CONTEXT ( ( #15355, #30240, #20445 ) ) REPRESENTATION_CONTEXT ( 'NONE', 'WORKASPACE' ) );
#18274=PRESENTATION_STYLE_ASSIGNMENT (( #8598 ) ) ;
#18275=DIRECTION ( 'NONE',  ( 1.000000000000000000, 0.000000000000000000, -3.491481338843133355E-15 ) ) ;
#18335=DIRECTION ( 'NONE',  ( 1.000000000000000000, 0.000000000000000000, -3.491481338843133355E-15 ) ) ;
#18963=EDGE_CURVE ( 'NONE', #27700, #26979, #2650, .T. ) ;
#19218=LINE ( 'NONE', #30917, #2413 ) ;
#19224=DIRECTION ( 'NONE',  ( 0.000000000000000000, 0.000000000000000000, -1.000000000000000000 ) ) ;
#19421=ORIENTED_EDGE ( 'NONE', *, *, #17155, .F. ) ;
#19453=CIRCLE ( 'NONE', #17401, 1.375000000000001332 ) ;
#19736=ORIENTED_EDGE ( 'NONE', *, *, #17155, .T. ) ;
#20084=CARTESIAN_POINT ( 'NONE',  ( 64.00000000000001421, 1.163569835200988601E-28, -1.375000000000224931 ) ) ;
#20262=FACE_OUTER_BOUND ( 'NONE', #22123, .T. ) ;
#20441=CARTESIAN_POINT ( 'NONE',  ( 64.00000000000001421, 1.990051048615640789E-16, -1.625000000000225153 ) ) ;
#20445=( NAMED_UNIT ( * ) SI_UNIT ( $, .STERADIAN. ) SOLID_ANGLE_UNIT ( ) );
#20609=AXIS2_PLACEMENT_3D ( 'NONE', #20084, #14992, #14692 ) ;
#20661=SURFACE_STYLE_FILL_AREA ( #10981 ) ;
#20814=ORIENTED_EDGE ( 'NONE', *, *, #29742, .T. ) ;
#20904=CARTESIAN_POINT ( 'NONE',  ( 64.25000000000001421, 1.163569835200988601E-28, -2.243276760206714411E-13 ) ) ;
#21064=COLOUR_RGB ( '', 0.09019608, 0.27058824, 0.51372549) ;
#21153=CARTESIAN_POINT ( 'NONE',  ( 51.25000000000002132, 1.836970198722195229E-16, 1.374999999999822586 ) ) ;
#21237=FACE_OUTER_BOUND ( 'NONE', #1557, .T. ) ;
#21277=CARTESIAN_POINT ( 'NONE',  ( 64.25000000000001421, 1.163569835200988601E-28, -2.243276760206714411E-13 ) ) ;
#21323=VERTEX_POINT ( 'NONE', #28593 ) ;
#21447=ORIENTED_EDGE ( 'NONE', *, *, #24207, .T. ) ;
#21721=STYLED_ITEM ( 'NONE', ( #8236 ), #13430 ) ;
#21805=EDGE_CURVE ( 'NONE', #24382, #16231, #19453, .T. ) ;
#21888=CARTESIAN_POINT ( 'NONE',  ( 64.25000000000001421, 1.163569835200988601E-28, -1.375000000000225819 ) ) ;
#21978=DIRECTION ( 'NONE',  ( 1.000000000000000000, 0.000000000000000000, -3.491481338843133355E-15 ) ) ;
#22109=ORIENTED_EDGE ( 'NONE', *, *, #28141, .F. ) ;
#22123=EDGE_LOOP ( 'NONE', ( #7458, #6975 ) ) ;
#22137=CARTESIAN_POINT ( 'NONE',  ( 64.25000000000001421, 1.163569835200988601E-28, 1.624999999999777067 ) ) ;
#22142=DIRECTION ( 'NONE',  ( -3.491481338843133355E-15, 0.000000000000000000, -1.000000000000000000 ) ) ;
#22722=DIRECTION ( 'NONE',  ( 1.000000000000000000, 0.000000000000000000, -3.491481338843133355E-15 ) ) ;
#22815=DIRECTION ( 'NONE',  ( 0.000000000000000000, 0.000000000000000000, -1.000000000000000000 ) ) ;
#23018=FILL_AREA_STYLE_COLOUR ( '', #21064 ) ;
#23243=DIRECTION ( 'NONE',  ( -3.491481338843133355E-15, 0.000000000000000000, -1.000000000000000000 ) ) ;
#23324=CARTESIAN_POINT ( 'NONE',  ( 51.50000000000002132, 1.163569835200988601E-28, -1.798112889504214751E-13 ) ) ;
#23435=ORIENTED_EDGE ( 'NONE', *, *, #1502, .F. ) ;
#23472=CIRCLE ( 'NONE', #9826, 1.375000000000001332 ) ;
#23520=CARTESIAN_POINT ( 'NONE',  ( 51.50000000000002842, 1.163569835200988601E-28, 1.624999999999821920 ) ) ;
#23558=CIRCLE ( 'NONE', #11431, 1.625000000000001332 ) ;
#23572=DIRECTION ( 'NONE',  ( 1.000000000000000000, 0.000000000000000000, -3.491481338843133355E-15 ) ) ;
#23951=DIRECTION ( 'NONE',  ( -1.000000000000000000, -0.000000000000000000, 3.491481338843133750E-15 ) ) ;
#24075=UNCERTAINTY_MEASURE_WITH_UNIT (LENGTH_MEASURE( 1.000000000000000082E-05 ), #15355, 'distance_accuracy_value', 'NONE');
#24085=AXIS2_PLACEMENT_3D ( 'NONE', #14249, #25965, #27219 ) ;
#24207=EDGE_CURVE ( 'NONE', #16231, #24382, #13882, .T. ) ;
#24304=APPLICATION_CONTEXT ( 'automotive_design' ) ;
#24382=VERTEX_POINT ( 'NONE', #21888 ) ;
#24385=UNCERTAINTY_MEASURE_WITH_UNIT (LENGTH_MEASURE( 1.000000000000000082E-05 ), #13495, 'distance_accuracy_value', 'NONE');
#24485=FACE_OUTER_BOUND ( 'NONE', #2599, .T. ) ;
#24532=AXIS2_PLACEMENT_3D ( 'NONE', #3391, #22722, #13184 ) ;
#24533=VERTEX_POINT ( 'NONE', #21153 ) ;
#24640=ADVANCED_FACE ( 'NONE', ( #12069 ), #14274, .T. ) ;
#24934=ADVANCED_FACE ( 'NONE', ( #21237 ), #6330, .T. ) ;
#25061=FACE_OUTER_BOUND ( 'NONE', #16298, .T. ) ;
#25155=ADVANCED_FACE ( 'NONE', ( #20262 ), #8515, .F. ) ;
#25231=CARTESIAN_POINT ( 'NONE',  ( 51.50000000000002132, 1.163569835200988601E-28, -1.798112889504214751E-13 ) ) ;
#25332=FILL_AREA_STYLE_COLOUR ( '', #12573 ) ;
#25802=ORIENTED_EDGE ( 'NONE', *, *, #21805, .F. ) ;
#25965=DIRECTION ( 'NONE',  ( -1.000000000000000000, -0.000000000000000000, 3.491481338843133355E-15 ) ) ;
#25987=CARTESIAN_POINT ( 'NONE',  ( 0.000000000000000000, 0.000000000000000000, 0.000000000000000000 ) ) ;
#26113=DIRECTION ( 'NONE',  ( 1.000000000000000000, 0.000000000000000000, -3.491481338843133355E-15 ) ) ;
#26330=DIRECTION ( 'NONE',  ( 0.000000000000000000, -1.000000000000000000, -0.000000000000000000 ) ) ;
#26371=PRODUCT_DEFINITION ( 'UNKNOWN', '', #4040, #27522 ) ;
#26432=DIRECTION ( 'NONE',  ( -1.000000000000000000, -0.000000000000000000, 3.491481338843133355E-15 ) ) ;
#26666=CLOSED_SHELL ( 'NONE', ( #24934, #13303, #1496, #24640, #28970, #25155, #18022, #13077 ) ) ;
#26687=CIRCLE ( 'NONE', #1377, 1.625000000000001332 ) ;
#26792=DIRECTION ( 'NONE',  ( -4.270088556250598741E-15, 0.000000000000000000, -1.000000000000000000 ) ) ;
#26979=VERTEX_POINT ( 'NONE', #23520 ) ;
#27219=DIRECTION ( 'NONE',  ( -5.046468293750706671E-15, 0.000000000000000000, -1.000000000000000000 ) ) ;
#27250=( GEOMETRIC_REPRESENTATION_CONTEXT ( 3 ) GLOBAL_UNCERTAINTY_ASSIGNED_CONTEXT ( ( #18052 ) ) GLOBAL_UNIT_ASSIGNED_CONTEXT ( ( #15208, #3172, #17755 ) ) REPRESENTATION_CONTEXT ( 'NONE', 'WORKASPACE' ) );
#27377=ORIENTED_EDGE ( 'NONE', *, *, #12889, .F. ) ;
#27460=VERTEX_POINT ( 'NONE', #7323 ) ;
#27505=CARTESIAN_POINT ( 'NONE',  ( 51.25000000000001421, 1.163569835200988601E-28, -1.789384186157106949E-13 ) ) ;
#27522=PRODUCT_DEFINITION_CONTEXT ( 'detailed design', #30215, 'design' ) ;
#27671=CARTESIAN_POINT ( 'NONE',  ( 64.00000000000001421, 1.163569835200988601E-28, -2.234548056859606357E-13 ) ) ;
#27700=VERTEX_POINT ( 'NONE', #9354 ) ;
#28141=EDGE_CURVE ( 'NONE', #21323, #26979, #26687, .T. ) ;
#28202=CIRCLE ( 'NONE', #17034, 0.2500000000000000000 ) ;
#28337=PRODUCT_CONTEXT ( 'NONE', #24304, 'mechanical' ) ;
#28593=CARTESIAN_POINT ( 'NONE',  ( 51.50000000000001421, 1.990051048615613918E-16, -1.625000000000181188 ) ) ;
#28608=AXIS2_PLACEMENT_3D ( 'NONE', #21277, #30907, #7306 ) ;
#28659=DIRECTION ( 'NONE',  ( 0.000000000000000000, 0.000000000000000000, 1.000000000000000000 ) ) ;
#28751=DIRECTION ( 'NONE',  ( 0.000000000000000000, 1.224646799147353454E-16, 1.000000000000000000 ) ) ;
#28932=ORIENTED_EDGE ( 'NONE', *, *, #29742, .F. ) ;
#28970=ADVANCED_FACE ( 'NONE', ( #24485 ), #5496, .T. ) ;
#29206=AXIS2_PLACEMENT_3D ( 'NONE', #27671, #18335, #23243 ) ;
#29269=DIRECTION ( 'NONE',  ( 0.000000000000000000, 0.000000000000000000, -1.000000000000000000 ) ) ;
#29742=EDGE_CURVE ( 'NONE', #489, #24382, #12006, .T. ) ;
#30215=APPLICATION_CONTEXT ( 'automotive_design' ) ;
#30240=( NAMED_UNIT ( * ) PLANE_ANGLE_UNIT ( ) SI_UNIT ( $, .RADIAN. ) );
#30287=SURFACE_SIDE_STYLE ('',( #20661 ) ) ;
#30644=CIRCLE ( 'NONE', #1828, 0.2500000000000000000 ) ;
#30888=SHAPE_REPRESENTATION ( 'Eraser', ( #9018 ), #18167 ) ;
#30907=DIRECTION ( 'NONE',  ( -1.000000000000000000, -0.000000000000000000, 3.491481338843133750E-15 ) ) ;
#30917=CARTESIAN_POINT ( 'NONE',  ( 64.25000000000001421, 1.990051048615613918E-16, -1.625000000000225819 ) ) ;
#30940=EDGE_LOOP ( 'NONE', ( #7076, #9914, #22109, #10129 ) ) ;
#31109=CARTESIAN_POINT ( 'NONE',  ( 51.50000000000002842, 1.683889348828776048E-16, 1.374999999999821698 ) ) ;
ENDSEC;
END-ISO-10303-21;
